ISO-10303-21;
HEADER;
/* Generated by software containing ST-Developer
 * from STEP Tools, Inc. (www.steptools.com) 
 */

FILE_DESCRIPTION(
/* description */ ('Bell-crank linkage with push rods'),
/* implementation_level */ '2;1');

FILE_NAME(
/* name */ 'Pin keeper (3).step',
/* time_stamp */ '2026-10-28T03:25:15-07:00',
/* author */ (''),
/* organization */ (''),
/* preprocessor_version */ 'ST-DEVELOPER v20.2',
/* originating_system */ 'Autodesk Translation Framework v15.17.0.0',
/* authorisation */ '');

FILE_SCHEMA (('AUTOMOTIVE_DESIGN { 1 0 10303 214 3 1 1 }'));
ENDSEC;

DATA;
#10=MECHANICAL_DESIGN_GEOMETRIC_PRESENTATION_REPRESENTATION('',(#662),#16678);
#546=SHAPE_REPRESENTATION_RELATIONSHIP('SRR','None',#16968,#600);
#600=ADVANCED_BREP_SHAPE_REPRESENTATION('',(#722),#16673);
#662=STYLED_ITEM('',(#17291),#722);
#722=MANIFOLD_SOLID_BREP('Body1',#8854);
#952=FACE_BOUND('',#2476,.T.);
#953=FACE_BOUND('',#2478,.T.);
#1217=PLANE('',#10464);
#1218=PLANE('',#10465);
#1724=FACE_OUTER_BOUND('',#2473,.T.);
#1725=FACE_OUTER_BOUND('',#2474,.T.);
#1726=FACE_OUTER_BOUND('',#2475,.T.);
#1727=FACE_OUTER_BOUND('',#2477,.T.);
#2473=EDGE_LOOP('',(#7899,#7900,#7901,#7902));
#2474=EDGE_LOOP('',(#7903,#7904,#7905,#7906));
#2475=EDGE_LOOP('',(#7907));
#2476=EDGE_LOOP('',(#7908));
#2477=EDGE_LOOP('',(#7909));
#2478=EDGE_LOOP('',(#7910));
#3030=LINE('',#16277,#3579);
#3031=LINE('',#16283,#3580);
#3579=VECTOR('',#13140,0.225);
#3580=VECTOR('',#13147,0.5);
#4087=CIRCLE('',#10459,0.225);
#4088=CIRCLE('',#10460,0.225);
#4089=CIRCLE('',#10462,0.5);
#4090=CIRCLE('',#10463,0.5);
#4778=VERTEX_POINT('',#16274);
#4779=VERTEX_POINT('',#16276);
#4780=VERTEX_POINT('',#16280);
#4781=VERTEX_POINT('',#16282);
#5827=EDGE_CURVE('',#4778,#4778,#4087,.T.);
#5828=EDGE_CURVE('',#4778,#4779,#3030,.T.);
#5829=EDGE_CURVE('',#4779,#4779,#4088,.T.);
#5830=EDGE_CURVE('',#4780,#4780,#4089,.T.);
#5831=EDGE_CURVE('',#4780,#4781,#3031,.T.);
#5832=EDGE_CURVE('',#4781,#4781,#4090,.T.);
#7899=ORIENTED_EDGE('',*,*,#5827,.F.);
#7900=ORIENTED_EDGE('',*,*,#5828,.T.);
#7901=ORIENTED_EDGE('',*,*,#5829,.T.);
#7902=ORIENTED_EDGE('',*,*,#5828,.F.);
#7903=ORIENTED_EDGE('',*,*,#5830,.F.);
#7904=ORIENTED_EDGE('',*,*,#5831,.T.);
#7905=ORIENTED_EDGE('',*,*,#5832,.T.);
#7906=ORIENTED_EDGE('',*,*,#5831,.F.);
#7907=ORIENTED_EDGE('',*,*,#5830,.T.);
#7908=ORIENTED_EDGE('',*,*,#5827,.T.);
#7909=ORIENTED_EDGE('',*,*,#5832,.F.);
#7910=ORIENTED_EDGE('',*,*,#5829,.F.);
#8260=CYLINDRICAL_SURFACE('',#10458,0.225);
#8261=CYLINDRICAL_SURFACE('',#10461,0.5);
#8749=ADVANCED_FACE('',(#1724),#8260,.F.);
#8750=ADVANCED_FACE('',(#1725),#8261,.T.);
#8751=ADVANCED_FACE('',(#1726,#952),#1217,.T.);
#8752=ADVANCED_FACE('',(#1727,#953),#1218,.F.);
#8854=CLOSED_SHELL('',(#8749,#8750,#8751,#8752));
#10457=AXIS2_PLACEMENT_3D('',#16272,#13134,#13135);
#10458=AXIS2_PLACEMENT_3D('',#16273,#13136,#13137);
#10459=AXIS2_PLACEMENT_3D('',#16275,#13138,#13139);
#10460=AXIS2_PLACEMENT_3D('',#16278,#13141,#13142);
#10461=AXIS2_PLACEMENT_3D('',#16279,#13143,#13144);
#10462=AXIS2_PLACEMENT_3D('',#16281,#13145,#13146);
#10463=AXIS2_PLACEMENT_3D('',#16284,#13148,#13149);
#10464=AXIS2_PLACEMENT_3D('',#16285,#13150,#13151);
#10465=AXIS2_PLACEMENT_3D('',#16286,#13152,#13153);
#13134=DIRECTION('axis',(0.,0.,1.));
#13135=DIRECTION('refdir',(1.,0.,0.));
#13136=DIRECTION('center_axis',(0.,0.,1.));
#13137=DIRECTION('ref_axis',(1.,0.,0.));
#13138=DIRECTION('center_axis',(0.,0.,-1.));
#13139=DIRECTION('ref_axis',(1.,0.,0.));
#13140=DIRECTION('',(0.,0.,-1.));
#13141=DIRECTION('center_axis',(0.,0.,-1.));
#13142=DIRECTION('ref_axis',(1.,0.,0.));
#13143=DIRECTION('center_axis',(0.,0.,1.));
#13144=DIRECTION('ref_axis',(1.,0.,0.));
#13145=DIRECTION('center_axis',(0.,0.,1.));
#13146=DIRECTION('ref_axis',(1.,0.,0.));
#13147=DIRECTION('',(0.,0.,-1.));
#13148=DIRECTION('center_axis',(0.,0.,1.));
#13149=DIRECTION('ref_axis',(1.,0.,0.));
#13150=DIRECTION('center_axis',(0.,0.,1.));
#13151=DIRECTION('ref_axis',(1.,0.,0.));
#13152=DIRECTION('center_axis',(0.,0.,1.));
#13153=DIRECTION('ref_axis',(1.,0.,0.));
#16272=CARTESIAN_POINT('',(0.,0.,0.));
#16273=CARTESIAN_POINT('Origin',(4.,12.,8.1));
#16274=CARTESIAN_POINT('',(3.775,12.,8.3));
#16275=CARTESIAN_POINT('Origin',(4.,12.,8.3));
#16276=CARTESIAN_POINT('',(3.775,12.,8.1));
#16277=CARTESIAN_POINT('',(3.775,12.,8.1));
#16278=CARTESIAN_POINT('Origin',(4.,12.,8.1));
#16279=CARTESIAN_POINT('Origin',(4.,12.,8.1));
#16280=CARTESIAN_POINT('',(3.5,12.,8.3));
#16281=CARTESIAN_POINT('Origin',(4.,12.,8.3));
#16282=CARTESIAN_POINT('',(3.5,12.,8.1));
#16283=CARTESIAN_POINT('',(3.5,12.,8.1));
#16284=CARTESIAN_POINT('Origin',(4.,12.,8.1));
#16285=CARTESIAN_POINT('Origin',(4.,12.,8.3));
#16286=CARTESIAN_POINT('Origin',(4.,12.,8.1));
#16609=UNCERTAINTY_MEASURE_WITH_UNIT(LENGTH_MEASURE(0.001),#16679,
'DISTANCE_ACCURACY_VALUE',
'Maximum model space distance between geometric entities at asserted c
onnectivities');
#16614=UNCERTAINTY_MEASURE_WITH_UNIT(LENGTH_MEASURE(0.001),#16679,
'DISTANCE_ACCURACY_VALUE',
'Maximum model space distance between geometric entities at asserted c
onnectivities');
#16673=(
GEOMETRIC_REPRESENTATION_CONTEXT(3)
GLOBAL_UNCERTAINTY_ASSIGNED_CONTEXT((#16609))
GLOBAL_UNIT_ASSIGNED_CONTEXT((#16679,#16681,#16682))
REPRESENTATION_CONTEXT('','3D')
);
#16678=(
GEOMETRIC_REPRESENTATION_CONTEXT(3)
GLOBAL_UNCERTAINTY_ASSIGNED_CONTEXT((#16614))
GLOBAL_UNIT_ASSIGNED_CONTEXT((#16679,#16681,#16682))
REPRESENTATION_CONTEXT('','3D')
);
#16679=(
LENGTH_UNIT()
NAMED_UNIT(*)
SI_UNIT(.CENTI.,.METRE.)
);
#16681=(
NAMED_UNIT(*)
PLANE_ANGLE_UNIT()
SI_UNIT($,.RADIAN.)
);
#16682=(
NAMED_UNIT(*)
SI_UNIT($,.STERADIAN.)
SOLID_ANGLE_UNIT()
);
#16741=SHAPE_DEFINITION_REPRESENTATION(#16815,#16968);
#16815=PRODUCT_DEFINITION_SHAPE('',$,#17032);
#16968=SHAPE_REPRESENTATION('',(#10457),#16673);
#16973=PRODUCT_DEFINITION_CONTEXT('part definition',#17164,'design');
#17032=PRODUCT_DEFINITION('Pin keeper (3)','Pin keeper (3)',#17095,#16973);
#17095=PRODUCT_DEFINITION_FORMATION('',$,#17224);
#17164=APPLICATION_CONTEXT(
'Core Data for Automotive Mechanical Design Process');
#17165=PRODUCT_CONTEXT('part definition',#17164,'mechanical');
#17224=PRODUCT('Pin keeper (3)','Pin keeper (3)','Pin keeper (3)',(#17165));
#17285=COLOUR_RGB('Grey',0.48,0.52,0.57);
#17286=FILL_AREA_STYLE_COLOUR('',#17285);
#17287=FILL_AREA_STYLE('',(#17286));
#17288=SURFACE_STYLE_FILL_AREA(#17287);
#17289=SURFACE_SIDE_STYLE('',(#17288));
#17290=SURFACE_STYLE_USAGE(.BOTH.,#17289);
#17291=PRESENTATION_STYLE_ASSIGNMENT((#17290));
ENDSEC;
END-ISO-10303-21;
